ISO-10303-21;
HEADER;
FILE_DESCRIPTION (('STEP AP214'),
    '1' );
FILE_NAME ('roller axis assy_r2.step',
    '2026-10-24T11:01:53',
    ( '' ),
    ( '' ),
    'SwSTEP 2.0',
    'SolidWorks 2026',
    '' );
FILE_SCHEMA (( 'AUTOMOTIVE_DESIGN' ));
ENDSEC;

DATA;
#1=FACE_OUTER_BOUND ( 'NONE', #2167, .T. ) ;
#14=EDGE_CURVE ( 'NONE', #3511, #8141, #5542, .T. ) ;
#16=ORIENTED_EDGE ( 'NONE', *, *, #5135, .F. ) ;
#28=VECTOR ( 'NONE', #6395, 1000.000000000000000 ) ;
#29=LINE ( 'NONE', #6648, #3973 ) ;
#69=LINE ( 'NONE', #4867, #7268 ) ;
#71=CIRCLE ( 'NONE', #3416, 10.00000000000000000 ) ;
#73=CARTESIAN_POINT ( 'NONE',  ( 0.000000000000000000, 0.000000000000000000, 140.0000000000000000 ) ) ;
#76=AXIS2_PLACEMENT_3D ( 'NONE', #4160, #6813, #4641 ) ;
#78=ORIENTED_EDGE ( 'NONE', *, *, #2299, .F. ) ;
#90=ADVANCED_FACE ( 'NONE', ( #2733 ), #143, .T. ) ;
#92=DIRECTION ( 'NONE',  ( 1.000000000000000000, 0.000000000000000000, 0.000000000000000000 ) ) ;
#93=FACE_OUTER_BOUND ( 'NONE', #2661, .T. ) ;
#113=ORIENTED_EDGE ( 'NONE', *, *, #5446, .F. ) ;
#119=AXIS2_PLACEMENT_3D ( 'NONE', #4281, #2979, #6929 ) ;
#126=AXIS2_PLACEMENT_3D ( 'NONE', #2068, #2105, #1941 ) ;
#135=EDGE_LOOP ( 'NONE', ( #1108, #6424, #4835, #16 ) ) ;
#143=CYLINDRICAL_SURFACE ( 'NONE', #76, 20.00000000000000000 ) ;
#150=AXIS2_PLACEMENT_3D ( 'NONE', #5383, #907, #6207 ) ;
#161=DIRECTION ( 'NONE',  ( -1.000000000000000000, 0.000000000000000000, 0.000000000000000000 ) ) ;
#179=APPLICATION_CONTEXT ( 'automotive_design' ) ;
#183=AXIS2_PLACEMENT_3D ( 'NONE', #2227, #4879, #1572 ) ;
#236=ORIENTED_EDGE ( 'NONE', *, *, #2533, .T. ) ;
#273=LINE ( 'NONE', #2937, #2703 ) ;
#274=AXIS2_PLACEMENT_3D ( 'NONE', #7086, #7713, #1130 ) ;
#296=EDGE_LOOP ( 'NONE', ( #5180, #2362, #7003, #1502 ) ) ;
#310=AXIS2_PLACEMENT_3D ( 'NONE', #6705, #757, #2626 ) ;
#337=VERTEX_POINT ( 'NONE', #8267 ) ;
#344=CARTESIAN_POINT ( 'NONE',  ( 20.00000000000000000, 0.000000000000000000, 120.0000000000000142 ) ) ;
#356=CARTESIAN_POINT ( 'NONE',  ( 5.000000000000000000, -5.000000000000000000, -97.99999999999997158 ) ) ;
#378=EDGE_CURVE ( 'NONE', #2201, #8486, #3600, .T. ) ;
#412=ADVANCED_FACE ( 'NONE', ( #1906, #505 ), #7904, .T. ) ;
#430=LINE ( 'NONE', #3656, #7408 ) ;
#434=( GEOMETRIC_REPRESENTATION_CONTEXT ( 3 ) GLOBAL_UNCERTAINTY_ASSIGNED_CONTEXT ( ( #457 ) ) GLOBAL_UNIT_ASSIGNED_CONTEXT ( ( #1840, #2417, #5746 ) ) REPRESENTATION_CONTEXT ( 'NONE', 'WORKASPACE' ) );
#457=UNCERTAINTY_MEASURE_WITH_UNIT (LENGTH_MEASURE( 1.000000000000000082E-05 ), #1840, 'distance_accuracy_value', 'NONE');
#464=DIRECTION ( 'NONE',  ( 0.000000000000000000, 0.000000000000000000, 1.000000000000000000 ) ) ;
#471=( GEOMETRIC_REPRESENTATION_CONTEXT ( 3 ) GLOBAL_UNCERTAINTY_ASSIGNED_CONTEXT ( ( #1772 ) ) GLOBAL_UNIT_ASSIGNED_CONTEXT ( ( #1714, #488, #8462 ) ) REPRESENTATION_CONTEXT ( 'NONE', 'WORKASPACE' ) );
#488=( NAMED_UNIT ( * ) PLANE_ANGLE_UNIT ( ) SI_UNIT ( $, .RADIAN. ) );
#500=DIRECTION ( 'NONE',  ( 0.000000000000000000, 0.000000000000000000, 1.000000000000000000 ) ) ;
#505=FACE_OUTER_BOUND ( 'NONE', #2039, .T. ) ;
#526=DIRECTION ( 'NONE',  ( -1.734723475976806848E-16, 1.000000000000000000, 0.000000000000000000 ) ) ;
#528=SHAPE_REPRESENTATION_RELATIONSHIP ( 'NONE' , 'NONE' ,  #2984, #2539 ) ;
#538=CARTESIAN_POINT ( 'NONE',  ( -5.000000000000000000, -5.000000000000000000, 148.0000000000000284 ) ) ;
#555=DIRECTION ( 'NONE',  ( 0.000000000000000000, 1.000000000000000000, 0.000000000000000000 ) ) ;
#556=ORIENTED_EDGE ( 'NONE', *, *, #5443, .T. ) ;
#573=LINE ( 'NONE', #1972, #5544 ) ;
#576=LINE ( 'NONE', #1273, #5469 ) ;
#594=AXIS2_PLACEMENT_3D ( 'NONE', #3123, #464, #5764 ) ;
#595=FACE_OUTER_BOUND ( 'NONE', #7513, .T. ) ;
#618=DIRECTION ( 'NONE',  ( -1.734723475976806848E-16, 1.000000000000000000, 0.000000000000000000 ) ) ;
#661=EDGE_CURVE ( 'NONE', #7356, #2201, #5955, .T. ) ;
#672=CARTESIAN_POINT ( 'NONE',  ( 10.00000000000000000, 0.000000000000000000, 140.0000000000000000 ) ) ;
#676=ORIENTED_EDGE ( 'NONE', *, *, #5459, .T. ) ;
#683=CARTESIAN_POINT ( 'NONE',  ( 5.000000000000000000, 5.000000000000000000, -105.9999999999999858 ) ) ;
#731=CIRCLE ( 'NONE', #310, 20.00000000000000000 ) ;
#757=DIRECTION ( 'NONE',  ( -0.000000000000000000, -0.000000000000000000, 1.000000000000000000 ) ) ;
#801=CARTESIAN_POINT ( 'NONE',  ( 0.000000000000000000, 0.000000000000000000, 140.0000000000000000 ) ) ;
#828=ORIENTED_EDGE ( 'NONE', *, *, #3798, .T. ) ;
#839=DIRECTION ( 'NONE',  ( -1.000000000000000000, 1.734723475976806848E-16, -0.000000000000000000 ) ) ;
#868=CARTESIAN_POINT ( 'NONE',  ( 10.00000000000000000, 0.000000000000000000, -97.99999999999997158 ) ) ;
#886=CARTESIAN_POINT ( 'NONE',  ( -5.000000000000001776, 5.000000000000001776, 148.0000000000000284 ) ) ;
#888=CARTESIAN_POINT ( 'NONE',  ( -5.000000000000000000, -5.000000000000000000, 140.0000000000000000 ) ) ;
#894=ORIENTED_EDGE ( 'NONE', *, *, #3357, .F. ) ;
#907=DIRECTION ( 'NONE',  ( 0.000000000000000000, 0.000000000000000000, -1.000000000000000000 ) ) ;
#981=EDGE_CURVE ( 'NONE', #7356, #8085, #7140, .T. ) ;
#1066=ORIENTED_EDGE ( 'NONE', *, *, #5474, .F. ) ;
#1071=AXIS2_PLACEMENT_3D ( 'NONE', #1162, #2440, #3166 ) ;
#1091=CARTESIAN_POINT ( 'NONE',  ( 0.000000000000000000, 0.000000000000000000, 140.0000000000000000 ) ) ;
#1094=EDGE_CURVE ( 'NONE', #5639, #3374, #29, .T. ) ;
#1099=SURFACE_STYLE_FILL_AREA ( #3840 ) ;
#1108=ORIENTED_EDGE ( 'NONE', *, *, #5934, .F. ) ;
#1115=LINE ( 'NONE', #6375, #6752 ) ;
#1130=DIRECTION ( 'NONE',  ( 1.000000000000000000, 0.000000000000000000, 0.000000000000000000 ) ) ;
#1140=DIRECTION ( 'NONE',  ( 0.000000000000000000, 0.000000000000000000, 1.000000000000000000 ) ) ;
#1147=DIRECTION ( 'NONE',  ( 1.000000000000000000, 0.000000000000000000, 0.000000000000000000 ) ) ;
#1158=DIRECTION ( 'NONE',  ( 0.000000000000000000, -1.000000000000000000, 0.000000000000000000 ) ) ;
#1162=CARTESIAN_POINT ( 'NONE',  ( 0.000000000000000000, 0.000000000000000000, -97.99999999999997158 ) ) ;
#1166=LINE ( 'NONE', #5806, #2003 ) ;
#1182=DIRECTION ( 'NONE',  ( -0.000000000000000000, -0.000000000000000000, -1.000000000000000000 ) ) ;
#1184=ORIENTED_EDGE ( 'NONE', *, *, #3190, .F. ) ;
#1198=FACE_OUTER_BOUND ( 'NONE', #296, .T. ) ;
#1214=PRODUCT_CONTEXT ( 'NONE', #5844, 'mechanical' ) ;
#1246=PRODUCT_DEFINITION_CONTEXT ( 'detailed design', #179, 'design' ) ;
#1254=CARTESIAN_POINT ( 'NONE',  ( -10.00000000000000000, 1.224646799147353256E-15, -97.99999999999997158 ) ) ;
#1273=CARTESIAN_POINT ( 'NONE',  ( 5.000000000000000000, -5.000000000000000000, 148.0000000000000284 ) ) ;
#1277=CIRCLE ( 'NONE', #6137, 20.00000000000000000 ) ;
#1291=AXIS2_PLACEMENT_3D ( 'NONE', #4138, #3489, #161 ) ;
#1317=DIRECTION ( 'NONE',  ( 1.000000000000000000, 0.000000000000000000, -0.000000000000000000 ) ) ;
#1330=DIRECTION ( 'NONE',  ( -0.000000000000000000, 0.000000000000000000, 1.000000000000000000 ) ) ;
#1332=CARTESIAN_POINT ( 'NONE',  ( -10.00000000000000000, 1.224646799147353256E-15, 120.0000000000000000 ) ) ;
#1349=EDGE_LOOP ( 'NONE', ( #3392, #4034, #1184, #4779 ) ) ;
#1354=CARTESIAN_POINT ( 'NONE',  ( 5.000000000000000000, 5.000000000000000000, -105.9999999999999858 ) ) ;
#1359=FACE_OUTER_BOUND ( 'NONE', #4254, .T. ) ;
#1391=FACE_BOUND ( 'NONE', #1349, .T. ) ;
#1398=CARTESIAN_POINT ( 'NONE',  ( -5.000000000000000000, -5.000000000000000000, -105.9999999999999858 ) ) ;
#1405=EDGE_CURVE ( 'NONE', #3511, #5594, #71, .T. ) ;
#1416=PRODUCT_DEFINITION_SHAPE ( 'NONE', 'NONE',  #7502 ) ;
#1446=EDGE_LOOP ( 'NONE', ( #4645, #2394, #6555, #7740 ) ) ;
#1459=ADVANCED_FACE ( 'NONE', ( #595 ), #5978, .F. ) ;
#1485=VECTOR ( 'NONE', #5322, 1000.000000000000000 ) ;
#1502=ORIENTED_EDGE ( 'NONE', *, *, #981, .T. ) ;
#1542=LINE ( 'NONE', #3544, #3198 ) ;
#1551=ORIENTED_EDGE ( 'NONE', *, *, #4510, .T. ) ;
#1565=VERTEX_POINT ( 'NONE', #4035 ) ;
#1572=DIRECTION ( 'NONE',  ( -1.734723475976806848E-16, 1.000000000000000000, 0.000000000000000000 ) ) ;
#1574=CIRCLE ( 'NONE', #1291, 20.00000000000000000 ) ;
#1587=CARTESIAN_POINT ( 'NONE',  ( 0.000000000000000000, 0.000000000000000000, -105.9999999999999858 ) ) ;
#1590=ORIENTED_EDGE ( 'NONE', *, *, #7756, .T. ) ;
#1597=ORIENTED_EDGE ( 'NONE', *, *, #1405, .T. ) ;
#1634=ORIENTED_EDGE ( 'NONE', *, *, #1964, .T. ) ;
#1675=DIRECTION ( 'NONE',  ( -1.000000000000000000, 0.000000000000000000, 0.000000000000000000 ) ) ;
#1714=( LENGTH_UNIT ( ) NAMED_UNIT ( * ) SI_UNIT ( .MILLI., .METRE. ) );
#1751=EDGE_CURVE ( 'NONE', #4177, #3374, #7031, .T. ) ;
#1771=CARTESIAN_POINT ( 'NONE',  ( -10.00000000000000000, 1.224646799147353256E-15, -97.99999999999997158 ) ) ;
#1772=UNCERTAINTY_MEASURE_WITH_UNIT (LENGTH_MEASURE( 1.000000000000000082E-05 ), #1714, 'distance_accuracy_value', 'NONE');
#1784=CARTESIAN_POINT ( 'NONE',  ( -5.000000000000000000, -5.000000000000000000, 148.0000000000000284 ) ) ;
#1790=EDGE_CURVE ( 'NONE', #5594, #3913, #1115, .T. ) ;
#1805=FACE_OUTER_BOUND ( 'NONE', #7374, .T. ) ;
#1807=DIRECTION ( 'NONE',  ( 0.000000000000000000, 0.000000000000000000, 1.000000000000000000 ) ) ;
#1840=( LENGTH_UNIT ( ) NAMED_UNIT ( * ) SI_UNIT ( .MILLI., .METRE. ) );
#1843=DIRECTION ( 'NONE',  ( -1.000000000000000000, 0.000000000000000000, -0.000000000000000000 ) ) ;
#1860=AXIS2_PLACEMENT_3D ( 'NONE', #3692, #7707, #6995 ) ;
#1886=SURFACE_SIDE_STYLE ('',( #1099 ) ) ;
#1906=FACE_BOUND ( 'NONE', #8099, .T. ) ;
#1914=CARTESIAN_POINT ( 'NONE',  ( 5.000000000000000000, -5.000000000000000000, 140.0000000000000000 ) ) ;
#1916=CARTESIAN_POINT ( 'NONE',  ( 5.000000000000000000, -5.000000000000000000, 140.0000000000000000 ) ) ;
#1924=VECTOR ( 'NONE', #618, 1000.000000000000000 ) ;
#1941=DIRECTION ( 'NONE',  ( -1.000000000000000000, 0.000000000000000000, 0.000000000000000000 ) ) ;
#1954=AXIS2_PLACEMENT_3D ( 'NONE', #5830, #3022, #4451 ) ;
#1964=EDGE_CURVE ( 'NONE', #3298, #4682, #3897, .T. ) ;
#1972=CARTESIAN_POINT ( 'NONE',  ( 20.00000000000000000, 0.000000000000000000, -154.5685424949238040 ) ) ;
#1977=CARTESIAN_POINT ( 'NONE',  ( 0.000000000000000000, 0.000000000000000000, 120.0000000000000142 ) ) ;
#2003=VECTOR ( 'NONE', #5726, 1000.000000000000000 ) ;
#2036=ADVANCED_FACE ( 'NONE', ( #93 ), #2889, .T. ) ;
#2039=EDGE_LOOP ( 'NONE', ( #1597, #2190 ) ) ;
#2049=CARTESIAN_POINT ( 'NONE',  ( 0.000000000000000000, 0.000000000000000000, -97.99999999999997158 ) ) ;
#2068=CARTESIAN_POINT ( 'NONE',  ( 0.000000000000000000, 0.000000000000000000, -97.99999999999997158 ) ) ;
#2071=VECTOR ( 'NONE', #4881, 1000.000000000000000 ) ;
#2083=VECTOR ( 'NONE', #839, 1000.000000000000000 ) ;
#2088=VECTOR ( 'NONE', #1675, 1000.000000000000000 ) ;
#2105=DIRECTION ( 'NONE',  ( 0.000000000000000000, 0.000000000000000000, -1.000000000000000000 ) ) ;
#2130=CIRCLE ( 'NONE', #2421, 10.00000000000000000 ) ;
#2149=EDGE_CURVE ( 'NONE', #7520, #8365, #7323, .T. ) ;
#2154=DIRECTION ( 'NONE',  ( 1.734723475976806848E-16, -1.000000000000000000, -0.000000000000000000 ) ) ;
#2167=EDGE_LOOP ( 'NONE', ( #5720, #6981, #4273, #2232 ) ) ;
#2176=VECTOR ( 'NONE', #1158, 1000.000000000000000 ) ;
#2190=ORIENTED_EDGE ( 'NONE', *, *, #3925, .T. ) ;
#2201=VERTEX_POINT ( 'NONE', #8552 ) ;
#2227=CARTESIAN_POINT ( 'NONE',  ( -5.000000000000000000, -5.000000000000000000, 148.0000000000000284 ) ) ;
#2232=ORIENTED_EDGE ( 'NONE', *, *, #3645, .F. ) ;
#2255=VERTEX_POINT ( 'NONE', #5832 ) ;
#2267=EDGE_LOOP ( 'NONE', ( #5425, #7201 ) ) ;
#2288=AXIS2_PLACEMENT_3D ( 'NONE', #2049, #2653, #7966 ) ;
#2289=CARTESIAN_POINT ( 'NONE',  ( 5.000000000000000000, 5.000000000000000000, -97.99999999999997158 ) ) ;
#2299=EDGE_CURVE ( 'NONE', #3347, #4177, #3888, .T. ) ;
#2322=CARTESIAN_POINT ( 'NONE',  ( 0.000000000000000000, 0.000000000000000000, -77.99999999999997158 ) ) ;
#2328=DIRECTION ( 'NONE',  ( 1.734723475976806848E-16, -1.000000000000000000, -0.000000000000000000 ) ) ;
#2362=ORIENTED_EDGE ( 'NONE', *, *, #378, .F. ) ;
#2392=DIRECTION ( 'NONE',  ( -0.000000000000000000, -0.000000000000000000, -1.000000000000000000 ) ) ;
#2394=ORIENTED_EDGE ( 'NONE', *, *, #1790, .T. ) ;
#2396=EDGE_CURVE ( 'NONE', #7425, #337, #6657, .T. ) ;
#2408=DIRECTION ( 'NONE',  ( -1.000000000000000000, 0.000000000000000000, 0.000000000000000000 ) ) ;
#2417=( NAMED_UNIT ( * ) PLANE_ANGLE_UNIT ( ) SI_UNIT ( $, .RADIAN. ) );
#2421=AXIS2_PLACEMENT_3D ( 'NONE', #1091, #6309, #4310 ) ;
#2431=CARTESIAN_POINT ( 'NONE',  ( 10.00000000000000000, 0.000000000000000000, -97.99999999999997158 ) ) ;
#2432=DIRECTION ( 'NONE',  ( 1.000000000000000000, 0.000000000000000000, 0.000000000000000000 ) ) ;
#2440=DIRECTION ( 'NONE',  ( 0.000000000000000000, 0.000000000000000000, -1.000000000000000000 ) ) ;
#2458=EDGE_CURVE ( 'NONE', #7520, #3184, #2755, .T. ) ;
#2462=FACE_OUTER_BOUND ( 'NONE', #4150, .T. ) ;
#2471=CLOSED_SHELL ( 'NONE', ( #7255, #7833, #6353, #5712, #412, #2712, #6984, #1459, #4194, #2036, #5069, #6579, #90, #4652, #5361, #6607, #7854, #8488, #2888, #4408 ) ) ;
#2474=DIRECTION ( 'NONE',  ( -0.000000000000000000, -0.000000000000000000, 1.000000000000000000 ) ) ;
#2488=EDGE_CURVE ( 'NONE', #5639, #7425, #3535, .T. ) ;
#2492=EDGE_LOOP ( 'NONE', ( #7476, #3168, #5507, #6785 ) ) ;
#2498=AXIS2_PLACEMENT_3D ( 'NONE', #2499, #4483, #526 ) ;
#2499=CARTESIAN_POINT ( 'NONE',  ( -5.000000000000000000, -5.000000000000000000, -105.9999999999999858 ) ) ;
#2508=CARTESIAN_POINT ( 'NONE',  ( 10.00000000000000000, 0.000000000000000000, -97.99999999999997158 ) ) ;
#2521=CARTESIAN_POINT ( 'NONE',  ( -10.00000000000000000, 1.224646799147353256E-15, 140.0000000000000000 ) ) ;
#2533=EDGE_CURVE ( 'NONE', #5002, #7356, #8200, .T. ) ;
#2539=ADVANCED_BREP_SHAPE_REPRESENTATION ( '', ( #4703, #594 ), #471 ) ;
#2543=STYLED_ITEM('',(#8678),#4703);
#2551=AXIS2_PLACEMENT_3D ( 'NONE', #4595, #7208, #5980 ) ;
#2594=CARTESIAN_POINT ( 'NONE',  ( -5.000000000000000000, -5.000000000000000000, -97.99999999999997158 ) ) ;
#2626=DIRECTION ( 'NONE',  ( -1.000000000000000000, 0.000000000000000000, 0.000000000000000000 ) ) ;
#2627=FACE_BOUND ( 'NONE', #3355, .T. ) ;
#2632=LINE ( 'NONE', #4758, #3202 ) ;
#2653=DIRECTION ( 'NONE',  ( -0.000000000000000000, -0.000000000000000000, 1.000000000000000000 ) ) ;
#2661=EDGE_LOOP ( 'NONE', ( #7288, #6976, #6325, #3445 ) ) ;
#2665=DIRECTION ( 'NONE',  ( -0.000000000000000000, -0.000000000000000000, 1.000000000000000000 ) ) ;
#2675=AXIS2_PLACEMENT_3D ( 'NONE', #5143, #7807, #1843 ) ;
#2696=VECTOR ( 'NONE', #4418, 1000.000000000000000 ) ;
#2701=CARTESIAN_POINT ( 'NONE',  ( -20.00000000000000000, 2.449293598294706513E-15, 120.0000000000000142 ) ) ;
#2703=VECTOR ( 'NONE', #5757, 1000.000000000000000 ) ;
#2712=ADVANCED_FACE ( 'NONE', ( #6487 ), #7093, .F. ) ;
#2733=FACE_OUTER_BOUND ( 'NONE', #135, .T. ) ;
#2755=LINE ( 'NONE', #868, #6084 ) ;
#2834=ORIENTED_EDGE ( 'NONE', *, *, #2396, .F. ) ;
#2837=AXIS2_PLACEMENT_3D ( 'NONE', #6370, #7069, #2432 ) ;
#2888=ADVANCED_FACE ( 'NONE', ( #7354, #1391 ), #6037, .F. ) ;
#2889=PLANE ( 'NONE',  #4822 ) ;
#2937=CARTESIAN_POINT ( 'NONE',  ( 5.000000000000000000, 5.000000000000000000, -105.9999999999999858 ) ) ;
#2963=DIRECTION ( 'NONE',  ( -1.734723475976806848E-16, -1.000000000000000000, 0.000000000000000000 ) ) ;
#2969=CARTESIAN_POINT ( 'NONE',  ( 5.000000000000000000, -5.000000000000000000, -105.9999999999999858 ) ) ;
#2979=DIRECTION ( 'NONE',  ( 0.000000000000000000, 0.000000000000000000, 1.000000000000000000 ) ) ;
#2984=SHAPE_REPRESENTATION ( 'roller axis assy_r2', ( #594 ), #471 ) ;
#3022=DIRECTION ( 'NONE',  ( 0.000000000000000000, 1.000000000000000000, 0.000000000000000000 ) ) ;
#3035=CARTESIAN_POINT ( 'NONE',  ( 5.000000000000000000, 5.000000000000000000, -97.99999999999997158 ) ) ;
#3046=DIRECTION ( 'NONE',  ( -1.000000000000000000, 0.000000000000000000, 0.000000000000000000 ) ) ;
#3057=AXIS2_PLACEMENT_3D ( 'NONE', #73, #5174, #4521 ) ;
#3101=SURFACE_STYLE_USAGE ( .BOTH. , #1886 ) ;
#3109=VECTOR ( 'NONE', #555, 1000.000000000000000 ) ;
#3123=CARTESIAN_POINT ( 'NONE',  ( 0.000000000000000000, 0.000000000000000000, 0.000000000000000000 ) ) ;
#3149=DIRECTION ( 'NONE',  ( 1.000000000000000000, 0.000000000000000000, 0.000000000000000000 ) ) ;
#3166=DIRECTION ( 'NONE',  ( -1.000000000000000000, 0.000000000000000000, -0.000000000000000000 ) ) ;
#3168=ORIENTED_EDGE ( 'NONE', *, *, #3357, .T. ) ;
#3184=VERTEX_POINT ( 'NONE', #672 ) ;
#3185=FILL_AREA_STYLE_COLOUR ( '', #7411 ) ;
#3190=EDGE_CURVE ( 'NONE', #7290, #8085, #7286, .T. ) ;
#3198=VECTOR ( 'NONE', #3624, 1000.000000000000000 ) ;
#3202=VECTOR ( 'NONE', #4666, 1000.000000000000000 ) ;
#3231=DIRECTION ( 'NONE',  ( -1.000000000000000000, 0.000000000000000000, 0.000000000000000000 ) ) ;
#3294=VECTOR ( 'NONE', #3317, 1000.000000000000000 ) ;
#3295=EDGE_CURVE ( 'NONE', #6851, #7063, #6515, .T. ) ;
#3298=VERTEX_POINT ( 'NONE', #8339 ) ;
#3317=DIRECTION ( 'NONE',  ( 1.000000000000000000, 0.000000000000000000, 0.000000000000000000 ) ) ;
#3347=VERTEX_POINT ( 'NONE', #4147 ) ;
#3355=EDGE_LOOP ( 'NONE', ( #7819, #894 ) ) ;
#3357=EDGE_CURVE ( 'NONE', #8365, #7520, #6655, .T. ) ;
#3368=AXIS2_PLACEMENT_3D ( 'NONE', #6609, #4567, #3231 ) ;
#3374=VERTEX_POINT ( 'NONE', #356 ) ;
#3375=EDGE_CURVE ( 'NONE', #6933, #7290, #1542, .T. ) ;
#3392=ORIENTED_EDGE ( 'NONE', *, *, #4510, .F. ) ;
#3403=ORIENTED_EDGE ( 'NONE', *, *, #1405, .F. ) ;
#3416=AXIS2_PLACEMENT_3D ( 'NONE', #3825, #4343, #3046 ) ;
#3445=ORIENTED_EDGE ( 'NONE', *, *, #2488, .T. ) ;
#3446=FACE_OUTER_BOUND ( 'NONE', #4309, .T. ) ;
#3476=CARTESIAN_POINT ( 'NONE',  ( -5.000000000000001776, 5.000000000000001776, -97.99999999999997158 ) ) ;
#3477=EDGE_LOOP ( 'NONE', ( #6334, #3403, #6903, #556 ) ) ;
#3489=DIRECTION ( 'NONE',  ( -0.000000000000000000, -0.000000000000000000, 1.000000000000000000 ) ) ;
#3511=VERTEX_POINT ( 'NONE', #2508 ) ;
#3535=LINE ( 'NONE', #2969, #2071 ) ;
#3536=EDGE_LOOP ( 'NONE', ( #1551, #7264, #6541, #7043 ) ) ;
#3542=DIRECTION ( 'NONE',  ( -1.000000000000000000, 0.000000000000000000, 0.000000000000000000 ) ) ;
#3544=CARTESIAN_POINT ( 'NONE',  ( -5.000000000000001776, 5.000000000000001776, 140.0000000000000000 ) ) ;
#3548=ORIENTED_EDGE ( 'NONE', *, *, #7672, .F. ) ;
#3600=LINE ( 'NONE', #7515, #6199 ) ;
#3604=CARTESIAN_POINT ( 'NONE',  ( -20.00000000000000000, 2.449293598294706513E-15, -154.5685424949238040 ) ) ;
#3624=DIRECTION ( 'NONE',  ( -1.000000000000000000, 1.734723475976806848E-16, -0.000000000000000000 ) ) ;
#3626=ORIENTED_EDGE ( 'NONE', *, *, #5135, .T. ) ;
#3642=CYLINDRICAL_SURFACE ( 'NONE', #2288, 10.00000000000000000 ) ;
#3644=( GEOMETRIC_REPRESENTATION_CONTEXT ( 3 ) GLOBAL_UNCERTAINTY_ASSIGNED_CONTEXT ( ( #6061 ) ) GLOBAL_UNIT_ASSIGNED_CONTEXT ( ( #4534, #5593, #7612 ) ) REPRESENTATION_CONTEXT ( 'NONE', 'WORKASPACE' ) );
#3645=EDGE_CURVE ( 'NONE', #1565, #6851, #573, .T. ) ;
#3656=CARTESIAN_POINT ( 'NONE',  ( -5.000000000000001776, 5.000000000000001776, -97.99999999999997158 ) ) ;
#3659=VECTOR ( 'NONE', #4399, 1000.000000000000000 ) ;
#3692=CARTESIAN_POINT ( 'NONE',  ( 0.000000000000000000, 0.000000000000000000, -97.99999999999997158 ) ) ;
#3776=CARTESIAN_POINT ( 'NONE',  ( -5.000000000000001776, 5.000000000000001776, 140.0000000000000000 ) ) ;
#3790=ORIENTED_EDGE ( 'NONE', *, *, #4842, .F. ) ;
#3794=AXIS2_PLACEMENT_3D ( 'NONE', #801, #7499, #3542 ) ;
#3798=EDGE_CURVE ( 'NONE', #2255, #5002, #5489, .T. ) ;
#3825=CARTESIAN_POINT ( 'NONE',  ( 0.000000000000000000, 0.000000000000000000, -97.99999999999997158 ) ) ;
#3837=CARTESIAN_POINT ( 'NONE',  ( -5.000000000000000000, -5.000000000000000000, 148.0000000000000284 ) ) ;
#3840=FILL_AREA_STYLE ('',( #3185 ) ) ;
#3848=PLANE ( 'NONE',  #1954 ) ;
#3877=FACE_OUTER_BOUND ( 'NONE', #6525, .T. ) ;
#3888=LINE ( 'NONE', #1354, #8042 ) ;
#3897=LINE ( 'NONE', #2594, #1485 ) ;
#3903=CARTESIAN_POINT ( 'NONE',  ( -5.000000000000000000, -5.000000000000000000, -105.9999999999999858 ) ) ;
#3913=VERTEX_POINT ( 'NONE', #7898 ) ;
#3925=EDGE_CURVE ( 'NONE', #5594, #3511, #5414, .T. ) ;
#3929=ORIENTED_EDGE ( 'NONE', *, *, #5472, .T. ) ;
#3966=EDGE_CURVE ( 'NONE', #7425, #3298, #2632, .T. ) ;
#3973=VECTOR ( 'NONE', #6077, 1000.000000000000000 ) ;
#3984=CARTESIAN_POINT ( 'NONE',  ( -5.000000000000000000, -5.000000000000000000, 140.0000000000000000 ) ) ;
#4034=ORIENTED_EDGE ( 'NONE', *, *, #7283, .F. ) ;
#4035=CARTESIAN_POINT ( 'NONE',  ( 20.00000000000000000, 0.000000000000000000, -77.99999999999997158 ) ) ;
#4054=ORIENTED_EDGE ( 'NONE', *, *, #6383, .F. ) ;
#4061=AXIS2_PLACEMENT_3D ( 'NONE', #538, #4578, #7232 ) ;
#4096=EDGE_CURVE ( 'NONE', #3374, #3298, #8209, .T. ) ;
#4124=EDGE_LOOP ( 'NONE', ( #5871, #1590, #676, #5723 ) ) ;
#4138=CARTESIAN_POINT ( 'NONE',  ( 0.000000000000000000, 0.000000000000000000, -77.99999999999997158 ) ) ;
#4147=CARTESIAN_POINT ( 'NONE',  ( 5.000000000000000000, 5.000000000000000000, -105.9999999999999858 ) ) ;
#4150=EDGE_LOOP ( 'NONE', ( #3790, #8372 ) ) ;
#4160=CARTESIAN_POINT ( 'NONE',  ( 0.000000000000000000, 0.000000000000000000, -154.5685424949238040 ) ) ;
#4177=VERTEX_POINT ( 'NONE', #2289 ) ;
#4187=CARTESIAN_POINT ( 'NONE',  ( 5.000000000000000000, -5.000000000000000000, -97.99999999999997158 ) ) ;
#4194=ADVANCED_FACE ( 'NONE', ( #1805 ), #3848, .F. ) ;
#4212=DIRECTION ( 'NONE',  ( -0.000000000000000000, -0.000000000000000000, -1.000000000000000000 ) ) ;
#4219=ORIENTED_EDGE ( 'NONE', *, *, #1751, .T. ) ;
#4231=CARTESIAN_POINT ( 'NONE',  ( -5.000000000000001776, 5.000000000000001776, 148.0000000000000284 ) ) ;
#4254=EDGE_LOOP ( 'NONE', ( #4856, #5154, #8478, #3929 ) ) ;
#4273=ORIENTED_EDGE ( 'NONE', *, *, #3295, .F. ) ;
#4281=CARTESIAN_POINT ( 'NONE',  ( 0.000000000000000000, 0.000000000000000000, 120.0000000000000000 ) ) ;
#4301=FACE_OUTER_BOUND ( 'NONE', #4124, .T. ) ;
#4309=EDGE_LOOP ( 'NONE', ( #6401, #7789, #4734, #4963 ) ) ;
#4310=DIRECTION ( 'NONE',  ( -1.000000000000000000, 0.000000000000000000, 0.000000000000000000 ) ) ;
#4328=ORIENTED_EDGE ( 'NONE', *, *, #1751, .F. ) ;
#4343=DIRECTION ( 'NONE',  ( 0.000000000000000000, 0.000000000000000000, -1.000000000000000000 ) ) ;
#4348=FACE_OUTER_BOUND ( 'NONE', #2492, .T. ) ;
#4352=DIRECTION ( 'NONE',  ( 0.000000000000000000, 0.000000000000000000, -1.000000000000000000 ) ) ;
#4399=DIRECTION ( 'NONE',  ( -0.000000000000000000, -0.000000000000000000, -1.000000000000000000 ) ) ;
#4408=ADVANCED_FACE ( 'NONE', ( #4348 ), #4434, .T. ) ;
#4417=FACE_OUTER_BOUND ( 'NONE', #1446, .T. ) ;
#4418=DIRECTION ( 'NONE',  ( -0.000000000000000000, -0.000000000000000000, 1.000000000000000000 ) ) ;
#4428=VECTOR ( 'NONE', #2328, 1000.000000000000000 ) ;
#4434=CYLINDRICAL_SURFACE ( 'NONE', #274, 10.00000000000000000 ) ;
#4451=DIRECTION ( 'NONE',  ( 0.000000000000000000, -0.000000000000000000, 1.000000000000000000 ) ) ;
#4483=DIRECTION ( 'NONE',  ( 1.000000000000000000, 1.734723475976806848E-16, 0.000000000000000000 ) ) ;
#4510=EDGE_CURVE ( 'NONE', #8486, #6933, #8530, .T. ) ;
#4521=DIRECTION ( 'NONE',  ( -1.000000000000000000, 0.000000000000000000, -0.000000000000000000 ) ) ;
#4534=( LENGTH_UNIT ( ) NAMED_UNIT ( * ) SI_UNIT ( .MILLI., .METRE. ) );
#4551=FACE_OUTER_BOUND ( 'NONE', #3536, .T. ) ;
#4567=DIRECTION ( 'NONE',  ( 0.000000000000000000, 0.000000000000000000, -1.000000000000000000 ) ) ;
#4578=DIRECTION ( 'NONE',  ( 0.000000000000000000, 1.000000000000000000, 0.000000000000000000 ) ) ;
#4595=CARTESIAN_POINT ( 'NONE',  ( 5.000000000000000000, -5.000000000000000000, 148.0000000000000284 ) ) ;
#4622=DIRECTION ( 'NONE',  ( 0.000000000000000000, 0.000000000000000000, 1.000000000000000000 ) ) ;
#4641=DIRECTION ( 'NONE',  ( 1.000000000000000000, 0.000000000000000000, 0.000000000000000000 ) ) ;
#4645=ORIENTED_EDGE ( 'NONE', *, *, #3925, .F. ) ;
#4647=DIRECTION ( 'NONE',  ( 1.000000000000000000, -1.734723475976806848E-16, 0.000000000000000000 ) ) ;
#4652=ADVANCED_FACE ( 'NONE', ( #5466 ), #7347, .F. ) ;
#4657=DIRECTION ( 'NONE',  ( -0.000000000000000000, -0.000000000000000000, 1.000000000000000000 ) ) ;
#4666=DIRECTION ( 'NONE',  ( -0.000000000000000000, -0.000000000000000000, 1.000000000000000000 ) ) ;
#4682=VERTEX_POINT ( 'NONE', #3476 ) ;
#4703=MANIFOLD_SOLID_BREP ( 'Boss-Extrude4', #2471 ) ;
#4734=ORIENTED_EDGE ( 'NONE', *, *, #3798, .F. ) ;
#4758=CARTESIAN_POINT ( 'NONE',  ( -5.000000000000000000, -5.000000000000000000, -105.9999999999999858 ) ) ;
#4779=ORIENTED_EDGE ( 'NONE', *, *, #3375, .F. ) ;
#4813=VECTOR ( 'NONE', #8386, 1000.000000000000000 ) ;
#4822=AXIS2_PLACEMENT_3D ( 'NONE', #1587, #6096, #7372 ) ;
#4835=ORIENTED_EDGE ( 'NONE', *, *, #3645, .T. ) ;
#4842=EDGE_CURVE ( 'NONE', #1565, #6692, #731, .T. ) ;
#4856=ORIENTED_EDGE ( 'NONE', *, *, #3190, .T. ) ;
#4866=ORIENTED_EDGE ( 'NONE', *, *, #7672, .T. ) ;
#4867=CARTESIAN_POINT ( 'NONE',  ( 5.000000000000000000, 5.000000000000000000, 148.0000000000000284 ) ) ;
#4879=DIRECTION ( 'NONE',  ( 1.000000000000000000, 1.734723475976806848E-16, -0.000000000000000000 ) ) ;
#4881=DIRECTION ( 'NONE',  ( -1.000000000000000000, 0.000000000000000000, 0.000000000000000000 ) ) ;
#4963=ORIENTED_EDGE ( 'NONE', *, *, #5836, .T. ) ;
#4964=CARTESIAN_POINT ( 'NONE',  ( -5.000000000000001776, 5.000000000000001776, -105.9999999999999858 ) ) ;
#4991=AXIS2_PLACEMENT_3D ( 'NONE', #5274, #7943, #92 ) ;
#5002=VERTEX_POINT ( 'NONE', #886 ) ;
#5069=ADVANCED_FACE ( 'NONE', ( #5704, #2462 ), #5791, .T. ) ;
#5135=EDGE_CURVE ( 'NONE', #7063, #6851, #1277, .T. ) ;
#5143=CARTESIAN_POINT ( 'NONE',  ( 0.000000000000000000, 0.000000000000000000, -77.99999999999997158 ) ) ;
#5154=ORIENTED_EDGE ( 'NONE', *, *, #981, .F. ) ;
#5174=DIRECTION ( 'NONE',  ( 0.000000000000000000, 0.000000000000000000, -1.000000000000000000 ) ) ;
#5180=ORIENTED_EDGE ( 'NONE', *, *, #7283, .T. ) ;
#5182=AXIS2_PLACEMENT_3D ( 'NONE', #6083, #2963, #5612 ) ;
#5183=EDGE_CURVE ( 'NONE', #3913, #8141, #7123, .T. ) ;
#5190=AXIS2_PLACEMENT_3D ( 'NONE', #1977, #4622, #1317 ) ;
#5239=ORIENTED_EDGE ( 'NONE', *, *, #5443, .F. ) ;
#5270=FACE_OUTER_BOUND ( 'NONE', #5348, .T. ) ;
#5274=CARTESIAN_POINT ( 'NONE',  ( 0.000000000000000000, 0.000000000000000000, 120.0000000000000142 ) ) ;
#5316=PLANE ( 'NONE',  #183 ) ;
#5322=DIRECTION ( 'NONE',  ( -1.734723475976806848E-16, 1.000000000000000000, 0.000000000000000000 ) ) ;
#5348=EDGE_LOOP ( 'NONE', ( #7121, #3626 ) ) ;
#5361=ADVANCED_FACE ( 'NONE', ( #3446 ), #5436, .F. ) ;
#5376=EDGE_CURVE ( 'NONE', #6692, #1565, #1574, .T. ) ;
#5383=CARTESIAN_POINT ( 'NONE',  ( 0.000000000000000000, 0.000000000000000000, 148.0000000000000284 ) ) ;
#5401=DIRECTION ( 'NONE',  ( 0.000000000000000000, 0.000000000000000000, 1.000000000000000000 ) ) ;
#5414=CIRCLE ( 'NONE', #126, 10.00000000000000000 ) ;
#5425=ORIENTED_EDGE ( 'NONE', *, *, #7926, .F. ) ;
#5436=PLANE ( 'NONE',  #5182 ) ;
#5443=EDGE_CURVE ( 'NONE', #8141, #3913, #6005, .T. ) ;
#5446=EDGE_CURVE ( 'NONE', #4682, #4177, #430, .T. ) ;
#5459=EDGE_CURVE ( 'NONE', #7335, #3184, #2130, .T. ) ;
#5466=FACE_OUTER_BOUND ( 'NONE', #7755, .T. ) ;
#5469=VECTOR ( 'NONE', #7813, 1000.000000000000000 ) ;
#5472=EDGE_CURVE ( 'NONE', #5002, #7290, #6959, .T. ) ;
#5474=EDGE_CURVE ( 'NONE', #337, #3347, #7050, .T. ) ;
#5489=LINE ( 'NONE', #4231, #2083 ) ;
#5507=ORIENTED_EDGE ( 'NONE', *, *, #2458, .T. ) ;
#5542=LINE ( 'NONE', #2431, #4813 ) ;
#5544=VECTOR ( 'NONE', #5401, 1000.000000000000000 ) ;
#5560=ORIENTED_EDGE ( 'NONE', *, *, #3966, .T. ) ;
#5578=PRODUCT_DEFINITION_FORMATION_WITH_SPECIFIED_SOURCE ( 'ANY', '', #6690, .NOT_KNOWN. ) ;
#5579=ORIENTED_EDGE ( 'NONE', *, *, #1094, .F. ) ;
#5583=AXIS2_PLACEMENT_3D ( 'NONE', #7327, #500, #7195 ) ;
#5593=( NAMED_UNIT ( * ) PLANE_ANGLE_UNIT ( ) SI_UNIT ( $, .RADIAN. ) );
#5594=VERTEX_POINT ( 'NONE', #1254 ) ;
#5596=AXIS2_PLACEMENT_3D ( 'NONE', #2322, #4352, #2408 ) ;
#5612=DIRECTION ( 'NONE',  ( 1.000000000000000000, -1.734723475976806848E-16, 0.000000000000000000 ) ) ;
#5632=CARTESIAN_POINT ( 'NONE',  ( -5.000000000000001776, 5.000000000000001776, -105.9999999999999858 ) ) ;
#5639=VERTEX_POINT ( 'NONE', #7303 ) ;
#5703=ORIENTED_EDGE ( 'NONE', *, *, #1094, .T. ) ;
#5704=FACE_BOUND ( 'NONE', #7185, .T. ) ;
#5712=ADVANCED_FACE ( 'NONE', ( #5943 ), #3642, .T. ) ;
#5719=DIRECTION ( 'NONE',  ( -0.000000000000000000, -0.000000000000000000, 1.000000000000000000 ) ) ;
#5720=ORIENTED_EDGE ( 'NONE', *, *, #4842, .T. ) ;
#5723=ORIENTED_EDGE ( 'NONE', *, *, #2458, .F. ) ;
#5726=DIRECTION ( 'NONE',  ( 1.000000000000000000, 0.000000000000000000, 0.000000000000000000 ) ) ;
#5746=( NAMED_UNIT ( * ) SI_UNIT ( $, .STERADIAN. ) SOLID_ANGLE_UNIT ( ) );
#5757=DIRECTION ( 'NONE',  ( 0.000000000000000000, -1.000000000000000000, 0.000000000000000000 ) ) ;
#5764=DIRECTION ( 'NONE',  ( 1.000000000000000000, 0.000000000000000000, 0.000000000000000000 ) ) ;
#5791=PLANE ( 'NONE',  #2675 ) ;
#5792=AXIS2_PLACEMENT_3D ( 'NONE', #6407, #1807, #1147 ) ;
#5806=CARTESIAN_POINT ( 'NONE',  ( -5.000000000000000000, -5.000000000000000000, 140.0000000000000000 ) ) ;
#5814=ORIENTED_EDGE ( 'NONE', *, *, #4096, .T. ) ;
#5830=CARTESIAN_POINT ( 'NONE',  ( 5.000000000000000000, -5.000000000000000000, -105.9999999999999858 ) ) ;
#5832=CARTESIAN_POINT ( 'NONE',  ( 5.000000000000000000, 5.000000000000000000, 148.0000000000000284 ) ) ;
#5836=EDGE_CURVE ( 'NONE', #2255, #6933, #69, .T. ) ;
#5844=APPLICATION_CONTEXT ( 'automotive_design' ) ;
#5871=ORIENTED_EDGE ( 'NONE', *, *, #2149, .T. ) ;
#5923=CYLINDRICAL_SURFACE ( 'NONE', #5583, 20.00000000000000000 ) ;
#5933=CARTESIAN_POINT ( 'NONE',  ( 10.00000000000000000, 0.000000000000000000, 120.0000000000000000 ) ) ;
#5934=EDGE_CURVE ( 'NONE', #6692, #7063, #8444, .T. ) ;
#5937=ORIENTED_EDGE ( 'NONE', *, *, #1964, .F. ) ;
#5943=FACE_OUTER_BOUND ( 'NONE', #3477, .T. ) ;
#5955=LINE ( 'NONE', #8027, #3294 ) ;
#5978=PLANE ( 'NONE',  #6051 ) ;
#5980=DIRECTION ( 'NONE',  ( 0.000000000000000000, 0.000000000000000000, 1.000000000000000000 ) ) ;
#5986=STYLED_ITEM ( 'NONE', ( #7804 ), #2539 ) ;
#6005=CIRCLE ( 'NONE', #5596, 10.00000000000000000 ) ;
#6012=VECTOR ( 'NONE', #2474, 1000.000000000000000 ) ;
#6035=CARTESIAN_POINT ( 'NONE',  ( 5.000000000000000000, 5.000000000000000000, 140.0000000000000000 ) ) ;
#6037=PLANE ( 'NONE',  #3057 ) ;
#6051=AXIS2_PLACEMENT_3D ( 'NONE', #683, #7381, #1330 ) ;
#6061=UNCERTAINTY_MEASURE_WITH_UNIT (LENGTH_MEASURE( 1.000000000000000082E-05 ), #4534, 'distance_accuracy_value', 'NONE');
#6077=DIRECTION ( 'NONE',  ( -0.000000000000000000, -0.000000000000000000, 1.000000000000000000 ) ) ;
#6079=ORIENTED_EDGE ( 'NONE', *, *, #5183, .F. ) ;
#6083=CARTESIAN_POINT ( 'NONE',  ( -5.000000000000001776, 5.000000000000001776, 148.0000000000000284 ) ) ;
#6084=VECTOR ( 'NONE', #2665, 1000.000000000000000 ) ;
#6096=DIRECTION ( 'NONE',  ( 0.000000000000000000, 0.000000000000000000, -1.000000000000000000 ) ) ;
#6130=MECHANICAL_DESIGN_GEOMETRIC_PRESENTATION_REPRESENTATION('',(#2543),#3644);
#6137=AXIS2_PLACEMENT_3D ( 'NONE', #7680, #1140, #3149 ) ;
#6199=VECTOR ( 'NONE', #2392, 1000.000000000000000 ) ;
#6207=DIRECTION ( 'NONE',  ( -1.000000000000000000, 0.000000000000000000, -0.000000000000000000 ) ) ;
#6225=CARTESIAN_POINT ( 'NONE',  ( -5.000000000000000000, -5.000000000000000000, 148.0000000000000284 ) ) ;
#6309=DIRECTION ( 'NONE',  ( 0.000000000000000000, 0.000000000000000000, -1.000000000000000000 ) ) ;
#6316=EDGE_LOOP ( 'NONE', ( #1634, #3548, #2834, #5560 ) ) ;
#6325=ORIENTED_EDGE ( 'NONE', *, *, #6383, .T. ) ;
#6334=ORIENTED_EDGE ( 'NONE', *, *, #1790, .F. ) ;
#6353=ADVANCED_FACE ( 'NONE', ( #4417 ), #8345, .T. ) ;
#6370=CARTESIAN_POINT ( 'NONE',  ( 0.000000000000000000, 0.000000000000000000, -97.99999999999997158 ) ) ;
#6375=CARTESIAN_POINT ( 'NONE',  ( -10.00000000000000000, 1.224646799147353256E-15, -97.99999999999997158 ) ) ;
#6383=EDGE_CURVE ( 'NONE', #3347, #5639, #273, .T. ) ;
#6395=DIRECTION ( 'NONE',  ( 1.000000000000000000, -1.734723475976806848E-16, 0.000000000000000000 ) ) ;
#6401=ORIENTED_EDGE ( 'NONE', *, *, #3375, .T. ) ;
#6407=CARTESIAN_POINT ( 'NONE',  ( 0.000000000000000000, 0.000000000000000000, 120.0000000000000000 ) ) ;
#6424=ORIENTED_EDGE ( 'NONE', *, *, #5376, .T. ) ;
#6487=FACE_OUTER_BOUND ( 'NONE', #6316, .T. ) ;
#6506=EDGE_CURVE ( 'NONE', #2201, #2255, #576, .T. ) ;
#6515=CIRCLE ( 'NONE', #4991, 20.00000000000000000 ) ;
#6516=SHAPE_DEFINITION_REPRESENTATION ( #1416, #2984 ) ;
#6525=EDGE_LOOP ( 'NONE', ( #7911, #78, #1066, #4866 ) ) ;
#6541=ORIENTED_EDGE ( 'NONE', *, *, #6506, .F. ) ;
#6555=ORIENTED_EDGE ( 'NONE', *, *, #5183, .T. ) ;
#6579=ADVANCED_FACE ( 'NONE', ( #2627, #5270 ), #7940, .T. ) ;
#6607=ADVANCED_FACE ( 'NONE', ( #1359 ), #5316, .F. ) ;
#6609=CARTESIAN_POINT ( 'NONE',  ( 0.000000000000000000, 0.000000000000000000, -77.99999999999997158 ) ) ;
#6639=PLANE ( 'NONE',  #2551 ) ;
#6648=CARTESIAN_POINT ( 'NONE',  ( 5.000000000000000000, -5.000000000000000000, -105.9999999999999858 ) ) ;
#6655=CIRCLE ( 'NONE', #119, 10.00000000000000000 ) ;
#6657=LINE ( 'NONE', #1398, #1924 ) ;
#6690=PRODUCT ( 'roller axis assy_r2', 'roller axis assy_r2', '', ( #1214 ) ) ;
#6692=VERTEX_POINT ( 'NONE', #7533 ) ;
#6705=CARTESIAN_POINT ( 'NONE',  ( 0.000000000000000000, 0.000000000000000000, -77.99999999999997158 ) ) ;
#6752=VECTOR ( 'NONE', #5719, 1000.000000000000000 ) ;
#6785=ORIENTED_EDGE ( 'NONE', *, *, #7926, .T. ) ;
#6813=DIRECTION ( 'NONE',  ( 0.000000000000000000, 0.000000000000000000, 1.000000000000000000 ) ) ;
#6851=VERTEX_POINT ( 'NONE', #344 ) ;
#6903=ORIENTED_EDGE ( 'NONE', *, *, #14, .T. ) ;
#6926=CARTESIAN_POINT ( 'NONE',  ( 10.00000000000000000, 0.000000000000000000, -77.99999999999997158 ) ) ;
#6929=DIRECTION ( 'NONE',  ( 1.000000000000000000, 0.000000000000000000, 0.000000000000000000 ) ) ;
#6933=VERTEX_POINT ( 'NONE', #6035 ) ;
#6959=LINE ( 'NONE', #7005, #3659 ) ;
#6976=ORIENTED_EDGE ( 'NONE', *, *, #5474, .T. ) ;
#6979=LINE ( 'NONE', #5632, #6012 ) ;
#6981=ORIENTED_EDGE ( 'NONE', *, *, #5934, .T. ) ;
#6984=ADVANCED_FACE ( 'NONE', ( #3877 ), #7215, .F. ) ;
#6995=DIRECTION ( 'NONE',  ( 1.000000000000000000, 0.000000000000000000, 0.000000000000000000 ) ) ;
#7003=ORIENTED_EDGE ( 'NONE', *, *, #661, .F. ) ;
#7005=CARTESIAN_POINT ( 'NONE',  ( -5.000000000000001776, 5.000000000000001776, 148.0000000000000284 ) ) ;
#7031=LINE ( 'NONE', #3035, #2176 ) ;
#7043=ORIENTED_EDGE ( 'NONE', *, *, #378, .T. ) ;
#7050=LINE ( 'NONE', #4964, #28 ) ;
#7063=VERTEX_POINT ( 'NONE', #2701 ) ;
#7069=DIRECTION ( 'NONE',  ( -0.000000000000000000, -0.000000000000000000, 1.000000000000000000 ) ) ;
#7086=CARTESIAN_POINT ( 'NONE',  ( 0.000000000000000000, 0.000000000000000000, -97.99999999999997158 ) ) ;
#7093=PLANE ( 'NONE',  #2498 ) ;
#7121=ORIENTED_EDGE ( 'NONE', *, *, #3295, .T. ) ;
#7123=CIRCLE ( 'NONE', #3368, 10.00000000000000000 ) ;
#7140=LINE ( 'NONE', #3837, #7594 ) ;
#7185=EDGE_LOOP ( 'NONE', ( #5239, #6079 ) ) ;
#7195=DIRECTION ( 'NONE',  ( 1.000000000000000000, 0.000000000000000000, 0.000000000000000000 ) ) ;
#7201=ORIENTED_EDGE ( 'NONE', *, *, #5459, .F. ) ;
#7208=DIRECTION ( 'NONE',  ( -1.000000000000000000, 0.000000000000000000, 0.000000000000000000 ) ) ;
#7215=PLANE ( 'NONE',  #7989 ) ;
#7232=DIRECTION ( 'NONE',  ( 0.000000000000000000, -0.000000000000000000, 1.000000000000000000 ) ) ;
#7236=MECHANICAL_DESIGN_GEOMETRIC_PRESENTATION_REPRESENTATION('',(#5986),#434);
#7255=ADVANCED_FACE ( 'NONE', ( #4301 ), #7616, .T. ) ;
#7264=ORIENTED_EDGE ( 'NONE', *, *, #5836, .F. ) ;
#7268=VECTOR ( 'NONE', #4212, 1000.000000000000000 ) ;
#7283=EDGE_CURVE ( 'NONE', #8085, #8486, #1166, .T. ) ;
#7286=LINE ( 'NONE', #3984, #7353 ) ;
#7288=ORIENTED_EDGE ( 'NONE', *, *, #2396, .T. ) ;
#7290=VERTEX_POINT ( 'NONE', #3776 ) ;
#7303=CARTESIAN_POINT ( 'NONE',  ( 5.000000000000000000, -5.000000000000000000, -105.9999999999999858 ) ) ;
#7323=CIRCLE ( 'NONE', #5792, 10.00000000000000000 ) ;
#7327=CARTESIAN_POINT ( 'NONE',  ( 0.000000000000000000, 0.000000000000000000, -154.5685424949238040 ) ) ;
#7335=VERTEX_POINT ( 'NONE', #2521 ) ;
#7347=PLANE ( 'NONE',  #150 ) ;
#7353=VECTOR ( 'NONE', #2154, 1000.000000000000000 ) ;
#7354=FACE_OUTER_BOUND ( 'NONE', #2267, .T. ) ;
#7356=VERTEX_POINT ( 'NONE', #1784 ) ;
#7372=DIRECTION ( 'NONE',  ( -1.000000000000000000, 0.000000000000000000, -0.000000000000000000 ) ) ;
#7374=EDGE_LOOP ( 'NONE', ( #5814, #7869, #7803, #5703 ) ) ;
#7381=DIRECTION ( 'NONE',  ( -1.000000000000000000, 0.000000000000000000, -0.000000000000000000 ) ) ;
#7408=VECTOR ( 'NONE', #8367, 1000.000000000000000 ) ;
#7411=COLOUR_RGB ( '',0.8941176470588234615, 0.8941176470588234615, 0.8941176470588234615 ) ;
#7425=VERTEX_POINT ( 'NONE', #3903 ) ;
#7476=ORIENTED_EDGE ( 'NONE', *, *, #7756, .F. ) ;
#7499=DIRECTION ( 'NONE',  ( 0.000000000000000000, 0.000000000000000000, -1.000000000000000000 ) ) ;
#7502=PRODUCT_DEFINITION ( 'UNKNOWN', '', #5578, #1246 ) ;
#7513=EDGE_LOOP ( 'NONE', ( #4219, #5579, #4054, #8331 ) ) ;
#7515=CARTESIAN_POINT ( 'NONE',  ( 5.000000000000000000, -5.000000000000000000, 148.0000000000000284 ) ) ;
#7520=VERTEX_POINT ( 'NONE', #5933 ) ;
#7533=CARTESIAN_POINT ( 'NONE',  ( -20.00000000000000000, 2.449293598294706513E-15, -77.99999999999997158 ) ) ;
#7594=VECTOR ( 'NONE', #1182, 1000.000000000000000 ) ;
#7612=( NAMED_UNIT ( * ) SI_UNIT ( $, .STERADIAN. ) SOLID_ANGLE_UNIT ( ) );
#7615=DIRECTION ( 'NONE',  ( 0.000000000000000000, 0.000000000000000000, 1.000000000000000000 ) ) ;
#7616=CYLINDRICAL_SURFACE ( 'NONE', #1860, 10.00000000000000000 ) ;
#7645=ORIENTED_EDGE ( 'NONE', *, *, #661, .T. ) ;
#7672=EDGE_CURVE ( 'NONE', #337, #4682, #6979, .T. ) ;
#7680=CARTESIAN_POINT ( 'NONE',  ( 0.000000000000000000, 0.000000000000000000, 120.0000000000000142 ) ) ;
#7689=ORIENTED_EDGE ( 'NONE', *, *, #6506, .T. ) ;
#7707=DIRECTION ( 'NONE',  ( -0.000000000000000000, -0.000000000000000000, 1.000000000000000000 ) ) ;
#7713=DIRECTION ( 'NONE',  ( -0.000000000000000000, -0.000000000000000000, 1.000000000000000000 ) ) ;
#7736=LINE ( 'NONE', #1771, #2696 ) ;
#7740=ORIENTED_EDGE ( 'NONE', *, *, #14, .F. ) ;
#7755=EDGE_LOOP ( 'NONE', ( #7689, #828, #236, #7645 ) ) ;
#7756=EDGE_CURVE ( 'NONE', #8365, #7335, #7736, .T. ) ;
#7789=ORIENTED_EDGE ( 'NONE', *, *, #5472, .F. ) ;
#7803=ORIENTED_EDGE ( 'NONE', *, *, #2488, .F. ) ;
#7804=PRESENTATION_STYLE_ASSIGNMENT (( #3101 ) ) ;
#7807=DIRECTION ( 'NONE',  ( 0.000000000000000000, 0.000000000000000000, -1.000000000000000000 ) ) ;
#7813=DIRECTION ( 'NONE',  ( 0.000000000000000000, 1.000000000000000000, 0.000000000000000000 ) ) ;
#7814=PLANE ( 'NONE',  #4061 ) ;
#7819=ORIENTED_EDGE ( 'NONE', *, *, #2149, .F. ) ;
#7833=ADVANCED_FACE ( 'NONE', ( #1 ), #5923, .T. ) ;
#7854=ADVANCED_FACE ( 'NONE', ( #1198 ), #7814, .F. ) ;
#7869=ORIENTED_EDGE ( 'NONE', *, *, #3966, .F. ) ;
#7878=CARTESIAN_POINT ( 'NONE',  ( -5.000000000000001776, 5.000000000000001776, -105.9999999999999858 ) ) ;
#7898=CARTESIAN_POINT ( 'NONE',  ( -10.00000000000000000, 1.224646799147353256E-15, -77.99999999999997158 ) ) ;
#7904=PLANE ( 'NONE',  #1071 ) ;
#7911=ORIENTED_EDGE ( 'NONE', *, *, #5446, .T. ) ;
#7926=EDGE_CURVE ( 'NONE', #3184, #7335, #8245, .T. ) ;
#7940=PLANE ( 'NONE',  #5190 ) ;
#7943=DIRECTION ( 'NONE',  ( 0.000000000000000000, 0.000000000000000000, 1.000000000000000000 ) ) ;
#7946=ORIENTED_EDGE ( 'NONE', *, *, #4096, .F. ) ;
#7966=DIRECTION ( 'NONE',  ( 1.000000000000000000, 0.000000000000000000, 0.000000000000000000 ) ) ;
#7989=AXIS2_PLACEMENT_3D ( 'NONE', #7878, #8012, #4647 ) ;
#8012=DIRECTION ( 'NONE',  ( -1.734723475976806848E-16, -1.000000000000000000, 0.000000000000000000 ) ) ;
#8027=CARTESIAN_POINT ( 'NONE',  ( -5.000000000000000000, -5.000000000000000000, 148.0000000000000284 ) ) ;
#8042=VECTOR ( 'NONE', #4657, 1000.000000000000000 ) ;
#8085=VERTEX_POINT ( 'NONE', #888 ) ;
#8099=EDGE_LOOP ( 'NONE', ( #5937, #7946, #4328, #113 ) ) ;
#8141=VERTEX_POINT ( 'NONE', #6926 ) ;
#8200=LINE ( 'NONE', #6225, #4428 ) ;
#8209=LINE ( 'NONE', #4187, #2088 ) ;
#8245=CIRCLE ( 'NONE', #3794, 10.00000000000000000 ) ;
#8267=CARTESIAN_POINT ( 'NONE',  ( -5.000000000000001776, 5.000000000000001776, -105.9999999999999858 ) ) ;
#8293=VECTOR ( 'NONE', #7615, 1000.000000000000000 ) ;
#8331=ORIENTED_EDGE ( 'NONE', *, *, #2299, .T. ) ;
#8339=CARTESIAN_POINT ( 'NONE',  ( -5.000000000000000000, -5.000000000000000000, -97.99999999999997158 ) ) ;
#8345=CYLINDRICAL_SURFACE ( 'NONE', #2837, 10.00000000000000000 ) ;
#8365=VERTEX_POINT ( 'NONE', #1332 ) ;
#8367=DIRECTION ( 'NONE',  ( 1.000000000000000000, -1.734723475976806848E-16, 0.000000000000000000 ) ) ;
#8372=ORIENTED_EDGE ( 'NONE', *, *, #5376, .F. ) ;
#8386=DIRECTION ( 'NONE',  ( -0.000000000000000000, -0.000000000000000000, 1.000000000000000000 ) ) ;
#8444=LINE ( 'NONE', #3604, #8293 ) ;
#8462=( NAMED_UNIT ( * ) SI_UNIT ( $, .STERADIAN. ) SOLID_ANGLE_UNIT ( ) );
#8478=ORIENTED_EDGE ( 'NONE', *, *, #2533, .F. ) ;
#8486=VERTEX_POINT ( 'NONE', #1914 ) ;
#8488=ADVANCED_FACE ( 'NONE', ( #4551 ), #6639, .F. ) ;
#8530=LINE ( 'NONE', #1916, #3109 ) ;
#8552=CARTESIAN_POINT ( 'NONE',  ( 5.000000000000000000, -5.000000000000000000, 148.0000000000000284 ) ) ;
#8672=COLOUR_RGB('Off White',0.89,0.88,0.83);
#8673=FILL_AREA_STYLE_COLOUR('',#8672);
#8674=FILL_AREA_STYLE('',(#8673));
#8675=SURFACE_STYLE_FILL_AREA(#8674);
#8676=SURFACE_SIDE_STYLE('',(#8675));
#8677=SURFACE_STYLE_USAGE(.BOTH.,#8676);
#8678=PRESENTATION_STYLE_ASSIGNMENT((#8677));
ENDSEC;
END-ISO-10303-21;
